ISO-10303-21;
HEADER;
/* Generated by software containing ST-Developer
 * from STEP Tools, Inc. (www.steptools.com) 
 */

FILE_DESCRIPTION(
/* description */ (''),
/* implementation_level */ '2;1');

FILE_NAME(
/* name */ 'Coupling.step',
/* time_stamp */ '2026-10-22T16:03:28+06:00',
/* author */ (''),
/* organization */ (''),
/* preprocessor_version */ 'ST-DEVELOPER v20.2',
/* originating_system */ 'Autodesk Translation Framework v15.15.0.0',
/* authorisation */ '');

FILE_SCHEMA (('AUTOMOTIVE_DESIGN { 1 0 10303 214 3 1 1 }'));
ENDSEC;

DATA;
#10=MECHANICAL_DESIGN_GEOMETRIC_PRESENTATION_REPRESENTATION('',(#85),#6096);
#55=TOROIDAL_SURFACE('',#3790,12.,0.5);
#56=TOROIDAL_SURFACE('',#3800,12.,0.5);
#63=SHAPE_REPRESENTATION_RELATIONSHIP('SRR','None',#6138,#74);
#74=ADVANCED_BREP_SHAPE_REPRESENTATION('',(#96),#6086);
#85=STYLED_ITEM('',(#6248),#96);
#96=MANIFOLD_SOLID_BREP('Coupling',#3594);
#111=FACE_BOUND('',#539,.T.);
#112=FACE_BOUND('',#542,.T.);
#195=PLANE('',#3798);
#196=PLANE('',#3803);
#343=FACE_OUTER_BOUND('',#536,.T.);
#344=FACE_OUTER_BOUND('',#537,.T.);
#345=FACE_OUTER_BOUND('',#538,.T.);
#346=FACE_OUTER_BOUND('',#540,.T.);
#347=FACE_OUTER_BOUND('',#541,.T.);
#348=FACE_OUTER_BOUND('',#543,.T.);
#536=EDGE_LOOP('',(#2646,#2647,#2648,#2649,#2650));
#537=EDGE_LOOP('',(#2651,#2652,#2653,#2654,#2655,#2656));
#538=EDGE_LOOP('',(#2657));
#539=EDGE_LOOP('',(#2658));
#540=EDGE_LOOP('',(#2659,#2660,#2661,#2662,#2663));
#541=EDGE_LOOP('',(#2664));
#542=EDGE_LOOP('',(#2665));
#543=EDGE_LOOP('',(#2666,#2667,#2668,#2669));
#836=LINE('',#5324,#1215);
#837=LINE('',#5339,#1216);
#1215=VECTOR('',#4293,12.5);
#1216=VECTOR('',#4314,7.5);
#1500=CIRCLE('',#3791,12.);
#1501=CIRCLE('',#3792,0.5);
#1502=CIRCLE('',#3793,12.5);
#1503=CIRCLE('',#3794,12.5);
#1504=CIRCLE('',#3796,12.5);
#1505=CIRCLE('',#3797,12.5);
#1506=CIRCLE('',#3799,7.5);
#1507=CIRCLE('',#3801,0.5);
#1508=CIRCLE('',#3802,12.);
#1509=CIRCLE('',#3804,7.5);
#1674=VERTEX_POINT('',#5315);
#1675=VERTEX_POINT('',#5317);
#1676=VERTEX_POINT('',#5319);
#1677=VERTEX_POINT('',#5323);
#1678=VERTEX_POINT('',#5325);
#1679=VERTEX_POINT('',#5329);
#1680=VERTEX_POINT('',#5332);
#1681=VERTEX_POINT('',#5336);
#2035=EDGE_CURVE('',#1674,#1674,#1500,.T.);
#2036=EDGE_CURVE('',#1674,#1675,#1501,.T.);
#2037=EDGE_CURVE('',#1675,#1676,#1502,.T.);
#2038=EDGE_CURVE('',#1676,#1675,#1503,.T.);
#2039=EDGE_CURVE('',#1676,#1677,#836,.T.);
#2040=EDGE_CURVE('',#1678,#1677,#1504,.T.);
#2041=EDGE_CURVE('',#1677,#1678,#1505,.T.);
#2042=EDGE_CURVE('',#1679,#1679,#1506,.T.);
#2043=EDGE_CURVE('',#1678,#1680,#1507,.T.);
#2044=EDGE_CURVE('',#1680,#1680,#1508,.T.);
#2045=EDGE_CURVE('',#1681,#1681,#1509,.T.);
#2046=EDGE_CURVE('',#1679,#1681,#837,.T.);
#2646=ORIENTED_EDGE('',*,*,#2035,.T.);
#2647=ORIENTED_EDGE('',*,*,#2036,.T.);
#2648=ORIENTED_EDGE('',*,*,#2037,.T.);
#2649=ORIENTED_EDGE('',*,*,#2038,.T.);
#2650=ORIENTED_EDGE('',*,*,#2036,.F.);
#2651=ORIENTED_EDGE('',*,*,#2038,.F.);
#2652=ORIENTED_EDGE('',*,*,#2039,.T.);
#2653=ORIENTED_EDGE('',*,*,#2040,.F.);
#2654=ORIENTED_EDGE('',*,*,#2041,.F.);
#2655=ORIENTED_EDGE('',*,*,#2039,.F.);
#2656=ORIENTED_EDGE('',*,*,#2037,.F.);
#2657=ORIENTED_EDGE('',*,*,#2035,.F.);
#2658=ORIENTED_EDGE('',*,*,#2042,.T.);
#2659=ORIENTED_EDGE('',*,*,#2041,.T.);
#2660=ORIENTED_EDGE('',*,*,#2043,.T.);
#2661=ORIENTED_EDGE('',*,*,#2044,.T.);
#2662=ORIENTED_EDGE('',*,*,#2043,.F.);
#2663=ORIENTED_EDGE('',*,*,#2040,.T.);
#2664=ORIENTED_EDGE('',*,*,#2044,.F.);
#2665=ORIENTED_EDGE('',*,*,#2045,.F.);
#2666=ORIENTED_EDGE('',*,*,#2042,.F.);
#2667=ORIENTED_EDGE('',*,*,#2046,.T.);
#2668=ORIENTED_EDGE('',*,*,#2045,.T.);
#2669=ORIENTED_EDGE('',*,*,#2046,.F.);
#3372=CYLINDRICAL_SURFACE('',#3795,12.5);
#3373=CYLINDRICAL_SURFACE('',#3805,7.5);
#3450=ADVANCED_FACE('',(#343),#55,.T.);
#3451=ADVANCED_FACE('',(#344),#3372,.T.);
#3452=ADVANCED_FACE('',(#345,#111),#195,.T.);
#3453=ADVANCED_FACE('',(#346),#56,.T.);
#3454=ADVANCED_FACE('',(#347,#112),#196,.F.);
#3455=ADVANCED_FACE('',(#348),#3373,.F.);
#3594=CLOSED_SHELL('',(#3450,#3451,#3452,#3453,#3454,#3455));
#3789=AXIS2_PLACEMENT_3D('',#5313,#4279,#4280);
#3790=AXIS2_PLACEMENT_3D('',#5314,#4281,#4282);
#3791=AXIS2_PLACEMENT_3D('',#5316,#4283,#4284);
#3792=AXIS2_PLACEMENT_3D('',#5318,#4285,#4286);
#3793=AXIS2_PLACEMENT_3D('',#5320,#4287,#4288);
#3794=AXIS2_PLACEMENT_3D('',#5321,#4289,#4290);
#3795=AXIS2_PLACEMENT_3D('',#5322,#4291,#4292);
#3796=AXIS2_PLACEMENT_3D('',#5326,#4294,#4295);
#3797=AXIS2_PLACEMENT_3D('',#5327,#4296,#4297);
#3798=AXIS2_PLACEMENT_3D('',#5328,#4298,#4299);
#3799=AXIS2_PLACEMENT_3D('',#5330,#4300,#4301);
#3800=AXIS2_PLACEMENT_3D('',#5331,#4302,#4303);
#3801=AXIS2_PLACEMENT_3D('',#5333,#4304,#4305);
#3802=AXIS2_PLACEMENT_3D('',#5334,#4306,#4307);
#3803=AXIS2_PLACEMENT_3D('',#5335,#4308,#4309);
#3804=AXIS2_PLACEMENT_3D('',#5337,#4310,#4311);
#3805=AXIS2_PLACEMENT_3D('',#5338,#4312,#4313);
#4279=DIRECTION('axis',(0.,0.,1.));
#4280=DIRECTION('refdir',(1.,0.,0.));
#4281=DIRECTION('center_axis',(0.,1.,0.));
#4282=DIRECTION('ref_axis',(0.,0.,1.));
#4283=DIRECTION('center_axis',(0.,-1.,0.));
#4284=DIRECTION('ref_axis',(-1.,0.,0.));
#4285=DIRECTION('center_axis',(-1.,0.,1.22464679914735E-16));
#4286=DIRECTION('ref_axis',(-1.22464679914735E-16,0.,-1.));
#4287=DIRECTION('center_axis',(0.,1.,0.));
#4288=DIRECTION('ref_axis',(-1.,0.,0.));
#4289=DIRECTION('center_axis',(0.,1.,0.));
#4290=DIRECTION('ref_axis',(-1.,0.,0.));
#4291=DIRECTION('center_axis',(0.,1.,0.));
#4292=DIRECTION('ref_axis',(-1.,0.,0.));
#4293=DIRECTION('',(0.,-1.,0.));
#4294=DIRECTION('center_axis',(0.,-1.,0.));
#4295=DIRECTION('ref_axis',(-1.,0.,0.));
#4296=DIRECTION('center_axis',(0.,-1.,0.));
#4297=DIRECTION('ref_axis',(-1.,0.,0.));
#4298=DIRECTION('center_axis',(0.,1.,0.));
#4299=DIRECTION('ref_axis',(-1.,0.,0.));
#4300=DIRECTION('center_axis',(0.,-1.,0.));
#4301=DIRECTION('ref_axis',(-1.,0.,0.));
#4302=DIRECTION('center_axis',(0.,1.,0.));
#4303=DIRECTION('ref_axis',(0.,0.,1.));
#4304=DIRECTION('center_axis',(-1.,0.,1.22464679914735E-16));
#4305=DIRECTION('ref_axis',(-1.22464679914735E-16,0.,-1.));
#4306=DIRECTION('center_axis',(0.,1.,0.));
#4307=DIRECTION('ref_axis',(-1.,0.,0.));
#4308=DIRECTION('center_axis',(0.,1.,0.));
#4309=DIRECTION('ref_axis',(-1.,0.,0.));
#4310=DIRECTION('center_axis',(0.,-1.,0.));
#4311=DIRECTION('ref_axis',(-1.,0.,0.));
#4312=DIRECTION('center_axis',(0.,1.,0.));
#4313=DIRECTION('ref_axis',(-1.,0.,0.));
#4314=DIRECTION('',(0.,-1.,0.));
#5313=CARTESIAN_POINT('',(0.,0.,0.));
#5314=CARTESIAN_POINT('Origin',(4.44089209850063E-15,581.925982185852,41.5000000000007));
#5315=CARTESIAN_POINT('',(2.9713159395238E-15,582.425982185852,29.5000000000007));
#5316=CARTESIAN_POINT('Origin',(4.44089209850063E-15,582.425982185852,41.5000000000007));
#5317=CARTESIAN_POINT('',(2.91008359956643E-15,581.925982185852,29.0000000000007));
#5318=CARTESIAN_POINT('Origin',(2.9713159395238E-15,581.925982185852,29.5000000000007));
#5319=CARTESIAN_POINT('',(12.5,581.925982185852,41.5000000000007));
#5320=CARTESIAN_POINT('Origin',(4.44089209850063E-15,581.925982185852,41.5000000000007));
#5321=CARTESIAN_POINT('Origin',(4.44089209850063E-15,581.925982185852,41.5000000000007));
#5322=CARTESIAN_POINT('Origin',(4.44089209850063E-15,552.425982185852,41.5000000000007));
#5323=CARTESIAN_POINT('',(12.5,552.925982185852,41.5000000000007));
#5324=CARTESIAN_POINT('',(12.5,552.425982185852,41.5000000000007));
#5325=CARTESIAN_POINT('',(2.91008359956643E-15,552.925982185852,29.0000000000007));
#5326=CARTESIAN_POINT('Origin',(4.44089209850063E-15,552.925982185852,41.5000000000007));
#5327=CARTESIAN_POINT('Origin',(4.44089209850063E-15,552.925982185852,41.5000000000007));
#5328=CARTESIAN_POINT('Origin',(4.44089209850063E-15,582.425982185852,41.5000000000007));
#5329=CARTESIAN_POINT('',(7.5,582.425982185852,41.5000000000007));
#5330=CARTESIAN_POINT('Origin',(4.44089209850063E-15,582.425982185852,41.5000000000007));
#5331=CARTESIAN_POINT('Origin',(4.44089209850063E-15,552.925982185852,41.5000000000007));
#5332=CARTESIAN_POINT('',(2.9713159395238E-15,552.425982185852,29.5000000000007));
#5333=CARTESIAN_POINT('Origin',(2.9713159395238E-15,552.925982185852,29.5000000000007));
#5334=CARTESIAN_POINT('Origin',(4.44089209850063E-15,552.425982185852,41.5000000000007));
#5335=CARTESIAN_POINT('Origin',(4.44089209850063E-15,552.425982185852,41.5000000000007));
#5336=CARTESIAN_POINT('',(7.5,552.425982185852,41.5000000000007));
#5337=CARTESIAN_POINT('Origin',(4.44089209850063E-15,552.425982185852,41.5000000000007));
#5338=CARTESIAN_POINT('Origin',(4.44089209850063E-15,552.425982185852,41.5000000000007));
#5339=CARTESIAN_POINT('',(7.5,552.425982185852,41.5000000000007));
#6073=UNCERTAINTY_MEASURE_WITH_UNIT(LENGTH_MEASURE(0.01),#6097,
'DISTANCE_ACCURACY_VALUE',
'Maximum model space distance between geometric entities at asserted c
onnectivities');
#6083=UNCERTAINTY_MEASURE_WITH_UNIT(LENGTH_MEASURE(0.01),#6097,
'DISTANCE_ACCURACY_VALUE',
'Maximum model space distance between geometric entities at asserted c
onnectivities');
#6086=(
GEOMETRIC_REPRESENTATION_CONTEXT(3)
GLOBAL_UNCERTAINTY_ASSIGNED_CONTEXT((#6073))
GLOBAL_UNIT_ASSIGNED_CONTEXT((#6097,#6099,#6100))
REPRESENTATION_CONTEXT('','3D')
);
#6096=(
GEOMETRIC_REPRESENTATION_CONTEXT(3)
GLOBAL_UNCERTAINTY_ASSIGNED_CONTEXT((#6083))
GLOBAL_UNIT_ASSIGNED_CONTEXT((#6097,#6099,#6100))
REPRESENTATION_CONTEXT('','3D')
);
#6097=(
LENGTH_UNIT()
NAMED_UNIT(*)
SI_UNIT(.MILLI.,.METRE.)
);
#6099=(
NAMED_UNIT(*)
PLANE_ANGLE_UNIT()
SI_UNIT($,.RADIAN.)
);
#6100=(
NAMED_UNIT(*)
SI_UNIT($,.STERADIAN.)
SOLID_ANGLE_UNIT()
);
#6103=SHAPE_DEFINITION_REPRESENTATION(#6115,#6138);
#6115=PRODUCT_DEFINITION_SHAPE('',$,#6151);
#6138=SHAPE_REPRESENTATION('',(#3789),#6086);
#6148=PRODUCT_DEFINITION_CONTEXT('part definition',#6186,'design');
#6151=PRODUCT_DEFINITION('Coupling','Coupling',#6163,#6148);
#6163=PRODUCT_DEFINITION_FORMATION('',$,#6190);
#6186=APPLICATION_CONTEXT(
'Core Data for Automotive Mechanical Design Process');
#6187=PRODUCT_CONTEXT('part definition',#6186,'mechanical');
#6190=PRODUCT('Coupling','Coupling',$,(#6187));
#6242=COLOUR_RGB('Sky Blue',0.24,0.69,0.87);
#6243=FILL_AREA_STYLE_COLOUR('',#6242);
#6244=FILL_AREA_STYLE('',(#6243));
#6245=SURFACE_STYLE_FILL_AREA(#6244);
#6246=SURFACE_SIDE_STYLE('',(#6245));
#6247=SURFACE_STYLE_USAGE(.BOTH.,#6246);
#6248=PRESENTATION_STYLE_ASSIGNMENT((#6247));
ENDSEC;
END-ISO-10303-21;
